ISO-10303-21;
HEADER;
/* Generated by software containing ST-Developer
 * from STEP Tools, Inc. (www.steptools.com) 
 */

FILE_DESCRIPTION(
/* description */ ('Manual piston pump'),
/* implementation_level */ '2;1');

FILE_NAME(
/* name */ 'Cap Screw - M5x20.step',
/* time_stamp */ '2026-11-02T16:54:23-08:00',
/* author */ (''),
/* organization */ (''),
/* preprocessor_version */ 'ST-DEVELOPER v20.2',
/* originating_system */ 'Autodesk Translation Framework v15.17.0.0',
/* authorisation */ '');

FILE_SCHEMA (('AUTOMOTIVE_DESIGN { 1 0 10303 214 3 1 1 }'));
ENDSEC;

DATA;
#10=MECHANICAL_DESIGN_GEOMETRIC_PRESENTATION_REPRESENTATION('',(#701),#19043);
#522=ORIENTED_CLOSED_SHELL('',*,#9486,.F.);
#527=CONICAL_SURFACE('',#10480,0.4,0.785398163397448);
#528=CONICAL_SURFACE('',#10484,0.41,0.785398163397448);
#529=CONICAL_SURFACE('',#10488,0.26,0.463647609000806);
#530=CONICAL_SURFACE('',#10492,0.225,0.785398163397448);
#553=BREP_WITH_VOIDS('Body1',#9485,(#522));
#575=SHAPE_REPRESENTATION_RELATIONSHIP('SRR','None',#19321,#638);
#638=ADVANCED_BREP_SHAPE_REPRESENTATION('',(#553),#18988);
#701=STYLED_ITEM('',(#19663),#553);
#884=FACE_BOUND('',#2042,.T.);
#1142=CYLINDRICAL_SURFACE('',#10482,0.425);
#1143=CYLINDRICAL_SURFACE('',#10490,0.24505);
#1405=FACE_OUTER_BOUND('',#2037,.T.);
#1406=FACE_OUTER_BOUND('',#2038,.T.);
#1407=FACE_OUTER_BOUND('',#2039,.T.);
#1408=FACE_OUTER_BOUND('',#2040,.T.);
#1409=FACE_OUTER_BOUND('',#2041,.T.);
#1410=FACE_OUTER_BOUND('',#2043,.T.);
#1411=FACE_OUTER_BOUND('',#2044,.T.);
#1412=FACE_OUTER_BOUND('',#2045,.T.);
#1413=FACE_OUTER_BOUND('',#2046,.T.);
#1414=FACE_OUTER_BOUND('',#2047,.T.);
#1415=FACE_OUTER_BOUND('',#2048,.T.);
#1416=FACE_OUTER_BOUND('',#2049,.T.);
#1417=FACE_OUTER_BOUND('',#2050,.T.);
#1418=FACE_OUTER_BOUND('',#2051,.T.);
#1419=FACE_OUTER_BOUND('',#2052,.T.);
#1420=FACE_OUTER_BOUND('',#2053,.T.);
#1421=FACE_OUTER_BOUND('',#2054,.T.);
#2037=EDGE_LOOP('',(#6735));
#2038=EDGE_LOOP('',(#6736,#6737,#6738,#6739));
#2039=EDGE_LOOP('',(#6740,#6741,#6742,#6743));
#2040=EDGE_LOOP('',(#6744,#6745,#6746,#6747));
#2041=EDGE_LOOP('',(#6748));
#2042=EDGE_LOOP('',(#6749));
#2043=EDGE_LOOP('',(#6750,#6751,#6752,#6753));
#2044=EDGE_LOOP('',(#6754,#6755,#6756,#6757));
#2045=EDGE_LOOP('',(#6758,#6759,#6760,#6761));
#2046=EDGE_LOOP('',(#6762));
#2047=EDGE_LOOP('',(#6763,#6764,#6765,#6766));
#2048=EDGE_LOOP('',(#6767,#6768,#6769,#6770));
#2049=EDGE_LOOP('',(#6771,#6772,#6773,#6774));
#2050=EDGE_LOOP('',(#6775,#6776,#6777,#6778));
#2051=EDGE_LOOP('',(#6779,#6780,#6781,#6782));
#2052=EDGE_LOOP('',(#6783,#6784,#6785,#6786));
#2053=EDGE_LOOP('',(#6787,#6788,#6789,#6790,#6791,#6792));
#2054=EDGE_LOOP('',(#6793,#6794,#6795,#6796,#6797,#6798));
#2769=CIRCLE('',#10479,0.375);
#2770=CIRCLE('',#10481,0.425);
#2771=CIRCLE('',#10483,0.425);
#2772=CIRCLE('',#10485,0.395);
#2773=CIRCLE('',#10487,0.27);
#2774=CIRCLE('',#10489,0.24505);
#2775=CIRCLE('',#10491,0.24505);
#2776=CIRCLE('',#10493,0.2);
#3269=LINE('',#15173,#3873);
#3270=LINE('',#15177,#3874);
#3271=LINE('',#15181,#3875);
#3272=LINE('',#15188,#3876);
#3273=LINE('',#15192,#3877);
#3274=LINE('',#15196,#3878);
#3275=LINE('',#15201,#3879);
#3276=LINE('',#15203,#3880);
#3277=LINE('',#15205,#3881);
#3278=LINE('',#15206,#3882);
#3279=LINE('',#15209,#3883);
#3280=LINE('',#15211,#3884);
#3281=LINE('',#15212,#3885);
#3282=LINE('',#15215,#3886);
#3283=LINE('',#15217,#3887);
#3284=LINE('',#15218,#3888);
#3285=LINE('',#15221,#3889);
#3286=LINE('',#15223,#3890);
#3287=LINE('',#15224,#3891);
#3288=LINE('',#15227,#3892);
#3289=LINE('',#15229,#3893);
#3290=LINE('',#15230,#3894);
#3291=LINE('',#15232,#3895);
#3292=LINE('',#15233,#3896);
#3873=VECTOR('',#12095,0.4);
#3874=VECTOR('',#12100,0.425);
#3875=VECTOR('',#12105,0.41);
#3876=VECTOR('',#12114,0.26);
#3877=VECTOR('',#12119,0.25);
#3878=VECTOR('',#12124,0.225);
#3879=VECTOR('',#12129,1.);
#3880=VECTOR('',#12130,1.);
#3881=VECTOR('',#12131,1.);
#3882=VECTOR('',#12132,1.);
#3883=VECTOR('',#12135,1.);
#3884=VECTOR('',#12136,1.);
#3885=VECTOR('',#12137,1.);
#3886=VECTOR('',#12140,1.);
#3887=VECTOR('',#12141,1.);
#3888=VECTOR('',#12142,1.);
#3889=VECTOR('',#12145,1.);
#3890=VECTOR('',#12146,1.);
#3891=VECTOR('',#12147,1.);
#3892=VECTOR('',#12150,1.);
#3893=VECTOR('',#12151,1.);
#3894=VECTOR('',#12152,1.);
#3895=VECTOR('',#12155,1.);
#3896=VECTOR('',#12156,1.);
#4508=VERTEX_POINT('',#15168);
#4509=VERTEX_POINT('',#15171);
#4510=VERTEX_POINT('',#15175);
#4511=VERTEX_POINT('',#15179);
#4512=VERTEX_POINT('',#15183);
#4513=VERTEX_POINT('',#15186);
#4514=VERTEX_POINT('',#15190);
#4515=VERTEX_POINT('',#15194);
#4516=VERTEX_POINT('',#15199);
#4517=VERTEX_POINT('',#15200);
#4518=VERTEX_POINT('',#15202);
#4519=VERTEX_POINT('',#15204);
#4520=VERTEX_POINT('',#15208);
#4521=VERTEX_POINT('',#15210);
#4522=VERTEX_POINT('',#15214);
#4523=VERTEX_POINT('',#15216);
#4524=VERTEX_POINT('',#15220);
#4525=VERTEX_POINT('',#15222);
#4526=VERTEX_POINT('',#15226);
#4527=VERTEX_POINT('',#15228);
#5354=EDGE_CURVE('',#4508,#4508,#2769,.T.);
#5355=EDGE_CURVE('',#4509,#4509,#2770,.T.);
#5356=EDGE_CURVE('',#4509,#4508,#3269,.T.);
#5357=EDGE_CURVE('',#4510,#4510,#2771,.T.);
#5358=EDGE_CURVE('',#4510,#4509,#3270,.T.);
#5359=EDGE_CURVE('',#4511,#4511,#2772,.T.);
#5360=EDGE_CURVE('',#4511,#4510,#3271,.T.);
#5361=EDGE_CURVE('',#4512,#4512,#2773,.T.);
#5362=EDGE_CURVE('',#4513,#4513,#2774,.F.);
#5363=EDGE_CURVE('',#4513,#4512,#3272,.T.);
#5364=EDGE_CURVE('',#4514,#4514,#2775,.F.);
#5365=EDGE_CURVE('',#4514,#4513,#3273,.T.);
#5366=EDGE_CURVE('',#4515,#4515,#2776,.T.);
#5367=EDGE_CURVE('',#4515,#4514,#3274,.T.);
#5368=EDGE_CURVE('',#4516,#4517,#3275,.T.);
#5369=EDGE_CURVE('',#4517,#4518,#3276,.T.);
#5370=EDGE_CURVE('',#4518,#4519,#3277,.T.);
#5371=EDGE_CURVE('',#4516,#4519,#3278,.T.);
#5372=EDGE_CURVE('',#4517,#4520,#3279,.T.);
#5373=EDGE_CURVE('',#4520,#4521,#3280,.T.);
#5374=EDGE_CURVE('',#4521,#4518,#3281,.T.);
#5375=EDGE_CURVE('',#4520,#4522,#3282,.T.);
#5376=EDGE_CURVE('',#4522,#4523,#3283,.T.);
#5377=EDGE_CURVE('',#4523,#4521,#3284,.T.);
#5378=EDGE_CURVE('',#4522,#4524,#3285,.T.);
#5379=EDGE_CURVE('',#4524,#4525,#3286,.T.);
#5380=EDGE_CURVE('',#4525,#4523,#3287,.T.);
#5381=EDGE_CURVE('',#4524,#4526,#3288,.T.);
#5382=EDGE_CURVE('',#4526,#4527,#3289,.T.);
#5383=EDGE_CURVE('',#4527,#4525,#3290,.T.);
#5384=EDGE_CURVE('',#4526,#4516,#3291,.T.);
#5385=EDGE_CURVE('',#4519,#4527,#3292,.T.);
#6735=ORIENTED_EDGE('',*,*,#5354,.F.);
#6736=ORIENTED_EDGE('',*,*,#5355,.F.);
#6737=ORIENTED_EDGE('',*,*,#5356,.T.);
#6738=ORIENTED_EDGE('',*,*,#5354,.T.);
#6739=ORIENTED_EDGE('',*,*,#5356,.F.);
#6740=ORIENTED_EDGE('',*,*,#5357,.F.);
#6741=ORIENTED_EDGE('',*,*,#5358,.T.);
#6742=ORIENTED_EDGE('',*,*,#5355,.T.);
#6743=ORIENTED_EDGE('',*,*,#5358,.F.);
#6744=ORIENTED_EDGE('',*,*,#5359,.F.);
#6745=ORIENTED_EDGE('',*,*,#5360,.T.);
#6746=ORIENTED_EDGE('',*,*,#5357,.T.);
#6747=ORIENTED_EDGE('',*,*,#5360,.F.);
#6748=ORIENTED_EDGE('',*,*,#5359,.T.);
#6749=ORIENTED_EDGE('',*,*,#5361,.F.);
#6750=ORIENTED_EDGE('',*,*,#5362,.F.);
#6751=ORIENTED_EDGE('',*,*,#5363,.T.);
#6752=ORIENTED_EDGE('',*,*,#5361,.T.);
#6753=ORIENTED_EDGE('',*,*,#5363,.F.);
#6754=ORIENTED_EDGE('',*,*,#5364,.F.);
#6755=ORIENTED_EDGE('',*,*,#5365,.T.);
#6756=ORIENTED_EDGE('',*,*,#5362,.T.);
#6757=ORIENTED_EDGE('',*,*,#5365,.F.);
#6758=ORIENTED_EDGE('',*,*,#5366,.F.);
#6759=ORIENTED_EDGE('',*,*,#5367,.T.);
#6760=ORIENTED_EDGE('',*,*,#5364,.T.);
#6761=ORIENTED_EDGE('',*,*,#5367,.F.);
#6762=ORIENTED_EDGE('',*,*,#5366,.T.);
#6763=ORIENTED_EDGE('',*,*,#5368,.T.);
#6764=ORIENTED_EDGE('',*,*,#5369,.T.);
#6765=ORIENTED_EDGE('',*,*,#5370,.T.);
#6766=ORIENTED_EDGE('',*,*,#5371,.F.);
#6767=ORIENTED_EDGE('',*,*,#5372,.T.);
#6768=ORIENTED_EDGE('',*,*,#5373,.T.);
#6769=ORIENTED_EDGE('',*,*,#5374,.T.);
#6770=ORIENTED_EDGE('',*,*,#5369,.F.);
#6771=ORIENTED_EDGE('',*,*,#5375,.T.);
#6772=ORIENTED_EDGE('',*,*,#5376,.T.);
#6773=ORIENTED_EDGE('',*,*,#5377,.T.);
#6774=ORIENTED_EDGE('',*,*,#5373,.F.);
#6775=ORIENTED_EDGE('',*,*,#5378,.T.);
#6776=ORIENTED_EDGE('',*,*,#5379,.T.);
#6777=ORIENTED_EDGE('',*,*,#5380,.T.);
#6778=ORIENTED_EDGE('',*,*,#5376,.F.);
#6779=ORIENTED_EDGE('',*,*,#5381,.T.);
#6780=ORIENTED_EDGE('',*,*,#5382,.T.);
#6781=ORIENTED_EDGE('',*,*,#5383,.T.);
#6782=ORIENTED_EDGE('',*,*,#5379,.F.);
#6783=ORIENTED_EDGE('',*,*,#5384,.T.);
#6784=ORIENTED_EDGE('',*,*,#5371,.T.);
#6785=ORIENTED_EDGE('',*,*,#5385,.T.);
#6786=ORIENTED_EDGE('',*,*,#5382,.F.);
#6787=ORIENTED_EDGE('',*,*,#5384,.F.);
#6788=ORIENTED_EDGE('',*,*,#5381,.F.);
#6789=ORIENTED_EDGE('',*,*,#5378,.F.);
#6790=ORIENTED_EDGE('',*,*,#5375,.F.);
#6791=ORIENTED_EDGE('',*,*,#5372,.F.);
#6792=ORIENTED_EDGE('',*,*,#5368,.F.);
#6793=ORIENTED_EDGE('',*,*,#5385,.F.);
#6794=ORIENTED_EDGE('',*,*,#5370,.F.);
#6795=ORIENTED_EDGE('',*,*,#5374,.F.);
#6796=ORIENTED_EDGE('',*,*,#5377,.F.);
#6797=ORIENTED_EDGE('',*,*,#5380,.F.);
#6798=ORIENTED_EDGE('',*,*,#5383,.F.);
#8634=PLANE('',#10478);
#8635=PLANE('',#10486);
#8636=PLANE('',#10494);
#8637=PLANE('',#10495);
#8638=PLANE('',#10496);
#8639=PLANE('',#10497);
#8640=PLANE('',#10498);
#8641=PLANE('',#10499);
#8642=PLANE('',#10500);
#8643=PLANE('',#10501);
#8644=PLANE('',#10502);
#9010=ADVANCED_FACE('',(#1405),#8634,.T.);
#9011=ADVANCED_FACE('',(#1406),#527,.T.);
#9012=ADVANCED_FACE('',(#1407),#1142,.T.);
#9013=ADVANCED_FACE('',(#1408),#528,.T.);
#9014=ADVANCED_FACE('',(#1409,#884),#8635,.T.);
#9015=ADVANCED_FACE('',(#1410),#529,.T.);
#9016=ADVANCED_FACE('',(#1411),#1143,.T.);
#9017=ADVANCED_FACE('',(#1412),#530,.T.);
#9018=ADVANCED_FACE('',(#1413),#8636,.T.);
#9019=ADVANCED_FACE('',(#1414),#8637,.F.);
#9020=ADVANCED_FACE('',(#1415),#8638,.F.);
#9021=ADVANCED_FACE('',(#1416),#8639,.F.);
#9022=ADVANCED_FACE('',(#1417),#8640,.F.);
#9023=ADVANCED_FACE('',(#1418),#8641,.F.);
#9024=ADVANCED_FACE('',(#1419),#8642,.F.);
#9025=ADVANCED_FACE('',(#1420),#8643,.F.);
#9026=ADVANCED_FACE('',(#1421),#8644,.F.);
#9485=CLOSED_SHELL('',(#9010,#9011,#9012,#9013,#9014,#9015,#9016,#9017,
#9018));
#9486=CLOSED_SHELL('',(#9019,#9020,#9021,#9022,#9023,#9024,#9025,#9026));
#10477=AXIS2_PLACEMENT_3D('',#15166,#12085,#12086);
#10478=AXIS2_PLACEMENT_3D('',#15167,#12087,#12088);
#10479=AXIS2_PLACEMENT_3D('',#15169,#12089,#12090);
#10480=AXIS2_PLACEMENT_3D('',#15170,#12091,#12092);
#10481=AXIS2_PLACEMENT_3D('',#15172,#12093,#12094);
#10482=AXIS2_PLACEMENT_3D('',#15174,#12096,#12097);
#10483=AXIS2_PLACEMENT_3D('',#15176,#12098,#12099);
#10484=AXIS2_PLACEMENT_3D('',#15178,#12101,#12102);
#10485=AXIS2_PLACEMENT_3D('',#15180,#12103,#12104);
#10486=AXIS2_PLACEMENT_3D('',#15182,#12106,#12107);
#10487=AXIS2_PLACEMENT_3D('',#15184,#12108,#12109);
#10488=AXIS2_PLACEMENT_3D('',#15185,#12110,#12111);
#10489=AXIS2_PLACEMENT_3D('',#15187,#12112,#12113);
#10490=AXIS2_PLACEMENT_3D('',#15189,#12115,#12116);
#10491=AXIS2_PLACEMENT_3D('',#15191,#12117,#12118);
#10492=AXIS2_PLACEMENT_3D('',#15193,#12120,#12121);
#10493=AXIS2_PLACEMENT_3D('',#15195,#12122,#12123);
#10494=AXIS2_PLACEMENT_3D('',#15197,#12125,#12126);
#10495=AXIS2_PLACEMENT_3D('',#15198,#12127,#12128);
#10496=AXIS2_PLACEMENT_3D('',#15207,#12133,#12134);
#10497=AXIS2_PLACEMENT_3D('',#15213,#12138,#12139);
#10498=AXIS2_PLACEMENT_3D('',#15219,#12143,#12144);
#10499=AXIS2_PLACEMENT_3D('',#15225,#12148,#12149);
#10500=AXIS2_PLACEMENT_3D('',#15231,#12153,#12154);
#10501=AXIS2_PLACEMENT_3D('',#15234,#12157,#12158);
#10502=AXIS2_PLACEMENT_3D('',#15235,#12159,#12160);
#12085=DIRECTION('axis',(0.,0.,1.));
#12086=DIRECTION('refdir',(1.,0.,0.));
#12087=DIRECTION('center_axis',(0.,1.,0.));
#12088=DIRECTION('ref_axis',(0.,0.,1.));
#12089=DIRECTION('center_axis',(0.,-1.,0.));
#12090=DIRECTION('ref_axis',(1.,0.,0.));
#12091=DIRECTION('center_axis',(0.,-1.,0.));
#12092=DIRECTION('ref_axis',(1.,0.,0.));
#12093=DIRECTION('center_axis',(0.,-1.,0.));
#12094=DIRECTION('ref_axis',(1.,0.,0.));
#12095=DIRECTION('',(0.707106781186548,0.707106781186547,8.65956056235493E-17));
#12096=DIRECTION('center_axis',(0.,-1.,0.));
#12097=DIRECTION('ref_axis',(1.,0.,0.));
#12098=DIRECTION('center_axis',(0.,-1.,0.));
#12099=DIRECTION('ref_axis',(1.,0.,0.));
#12100=DIRECTION('',(0.,1.,0.));
#12101=DIRECTION('center_axis',(0.,1.,0.));
#12102=DIRECTION('ref_axis',(1.,0.,0.));
#12103=DIRECTION('center_axis',(0.,-1.,0.));
#12104=DIRECTION('ref_axis',(1.,0.,0.));
#12105=DIRECTION('',(-0.707106781186547,0.707106781186548,-8.65956056235493E-17));
#12106=DIRECTION('center_axis',(0.,-1.,0.));
#12107=DIRECTION('ref_axis',(0.,0.,-1.));
#12108=DIRECTION('center_axis',(0.,-1.,0.));
#12109=DIRECTION('ref_axis',(1.,0.,0.));
#12110=DIRECTION('center_axis',(0.,1.,0.));
#12111=DIRECTION('ref_axis',(1.,0.,0.));
#12112=DIRECTION('center_axis',(0.,1.,0.));
#12113=DIRECTION('ref_axis',(1.,0.,0.));
#12114=DIRECTION('',(-0.447213595499958,0.894427190999916,-5.47678698264203E-17));
#12115=DIRECTION('center_axis',(0.,-1.,0.));
#12116=DIRECTION('ref_axis',(1.,0.,0.));
#12117=DIRECTION('center_axis',(0.,1.,0.));
#12118=DIRECTION('ref_axis',(1.,0.,0.));
#12119=DIRECTION('',(0.,1.,0.));
#12120=DIRECTION('center_axis',(0.,1.,0.));
#12121=DIRECTION('ref_axis',(1.,0.,0.));
#12122=DIRECTION('center_axis',(0.,-1.,0.));
#12123=DIRECTION('ref_axis',(1.,0.,0.));
#12124=DIRECTION('',(-0.707106781186547,0.707106781186548,-8.65956056235493E-17));
#12125=DIRECTION('center_axis',(0.,-1.,0.));
#12126=DIRECTION('ref_axis',(0.,0.,-1.));
#12127=DIRECTION('center_axis',(0.866025403784439,0.,-0.5));
#12128=DIRECTION('ref_axis',(0.5,0.,0.866025403784439));
#12129=DIRECTION('',(-0.5,0.,-0.866025403784439));
#12130=DIRECTION('',(0.,-1.,0.));
#12131=DIRECTION('',(0.5,0.,0.866025403784439));
#12132=DIRECTION('',(0.,-1.,0.));
#12133=DIRECTION('center_axis',(1.20185167898973E-16,0.,-1.));
#12134=DIRECTION('ref_axis',(1.,0.,1.20185167898973E-16));
#12135=DIRECTION('',(-1.,0.,-1.20185167898973E-16));
#12136=DIRECTION('',(0.,-1.,0.));
#12137=DIRECTION('',(1.,0.,1.20185167898973E-16));
#12138=DIRECTION('center_axis',(-0.866025403784439,0.,-0.5));
#12139=DIRECTION('ref_axis',(0.5,0.,-0.866025403784439));
#12140=DIRECTION('',(-0.5,0.,0.866025403784439));
#12141=DIRECTION('',(0.,-1.,0.));
#12142=DIRECTION('',(0.5,0.,-0.866025403784439));
#12143=DIRECTION('center_axis',(-0.866025403784439,0.,0.5));
#12144=DIRECTION('ref_axis',(-0.5,0.,-0.866025403784439));
#12145=DIRECTION('',(0.5,0.,0.866025403784439));
#12146=DIRECTION('',(0.,-1.,0.));
#12147=DIRECTION('',(-0.5,0.,-0.866025403784439));
#12148=DIRECTION('center_axis',(-2.40370335797945E-16,0.,1.));
#12149=DIRECTION('ref_axis',(-1.,0.,-2.40370335797945E-16));
#12150=DIRECTION('',(1.,0.,2.40370335797945E-16));
#12151=DIRECTION('',(0.,-1.,0.));
#12152=DIRECTION('',(-1.,0.,-2.40370335797945E-16));
#12153=DIRECTION('center_axis',(0.866025403784439,0.,0.5));
#12154=DIRECTION('ref_axis',(-0.5,0.,0.866025403784439));
#12155=DIRECTION('',(0.5,0.,-0.866025403784439));
#12156=DIRECTION('',(-0.5,0.,0.866025403784439));
#12157=DIRECTION('center_axis',(0.,1.,0.));
#12158=DIRECTION('ref_axis',(1.,0.,0.));
#12159=DIRECTION('center_axis',(0.,-1.,0.));
#12160=DIRECTION('ref_axis',(0.,0.,-1.));
#15166=CARTESIAN_POINT('',(0.,0.,0.));
#15167=CARTESIAN_POINT('Origin',(0.375,0.5,0.));
#15168=CARTESIAN_POINT('',(-0.375,0.5,-4.59242549680257E-17));
#15169=CARTESIAN_POINT('Origin',(0.,0.5,0.));
#15170=CARTESIAN_POINT('Origin',(0.,0.475,0.));
#15171=CARTESIAN_POINT('',(-0.425,0.45,-5.20474889637625E-17));
#15172=CARTESIAN_POINT('Origin',(0.,0.45,0.));
#15173=CARTESIAN_POINT('',(-0.4,0.475,-4.89858719658941E-17));
#15174=CARTESIAN_POINT('Origin',(0.,0.24,0.));
#15175=CARTESIAN_POINT('',(-0.425,0.0299999999999998,-5.20474889637625E-17));
#15176=CARTESIAN_POINT('Origin',(0.,0.0299999999999998,0.));
#15177=CARTESIAN_POINT('',(-0.425,0.24,-5.20474889637625E-17));
#15178=CARTESIAN_POINT('Origin',(0.,0.0150000000000001,0.));
#15179=CARTESIAN_POINT('',(-0.395,4.85722573273506E-17,-4.83735485663204E-17));
#15180=CARTESIAN_POINT('Origin',(0.,0.,0.));
#15181=CARTESIAN_POINT('',(-0.41,0.0150000000000001,-5.02105187650415E-17));
#15182=CARTESIAN_POINT('Origin',(0.27,0.,0.));
#15183=CARTESIAN_POINT('',(-0.27,0.,-3.30654635769785E-17));
#15184=CARTESIAN_POINT('Origin',(0.,0.,0.));
#15185=CARTESIAN_POINT('Origin',(0.,-0.02,0.));
#15186=CARTESIAN_POINT('',(-0.24505,-0.0498999999999999,3.00099698131059E-17));
#15187=CARTESIAN_POINT('Origin',(0.,-0.0498999999999999,0.));
#15188=CARTESIAN_POINT('',(-0.26,-0.02,-3.18408167778312E-17));
#15189=CARTESIAN_POINT('Origin',(0.,-0.995,0.));
#15190=CARTESIAN_POINT('',(-0.24505,-1.95495,3.00099698131059E-17));
#15191=CARTESIAN_POINT('Origin',(0.,-1.95495,0.));
#15192=CARTESIAN_POINT('',(-0.24505,-0.995,-3.00099698131059E-17));
#15193=CARTESIAN_POINT('Origin',(0.,-1.975,0.));
#15194=CARTESIAN_POINT('',(-0.2,-2.,-2.44929359829471E-17));
#15195=CARTESIAN_POINT('Origin',(0.,-2.,0.));
#15196=CARTESIAN_POINT('',(-0.225,-1.975,-2.75545529808154E-17));
#15197=CARTESIAN_POINT('Origin',(0.,-2.,0.));
#15198=CARTESIAN_POINT('Origin',(0.115470053837925,-0.5,-0.2));
#15199=CARTESIAN_POINT('',(0.23094010767585,-0.5,0.));
#15200=CARTESIAN_POINT('',(0.115470053837925,-0.5,-0.2));
#15201=CARTESIAN_POINT('',(0.23094010767585,-0.5,0.));
#15202=CARTESIAN_POINT('',(0.115470053837925,-0.8,-0.2));
#15203=CARTESIAN_POINT('',(0.115470053837925,-0.5,-0.2));
#15204=CARTESIAN_POINT('',(0.23094010767585,-0.8,0.));
#15205=CARTESIAN_POINT('',(0.23094010767585,-0.8,0.));
#15206=CARTESIAN_POINT('',(0.23094010767585,-0.5,0.));
#15207=CARTESIAN_POINT('Origin',(-0.115470053837925,-0.5,-0.2));
#15208=CARTESIAN_POINT('',(-0.115470053837925,-0.5,-0.2));
#15209=CARTESIAN_POINT('',(0.115470053837925,-0.5,-0.2));
#15210=CARTESIAN_POINT('',(-0.115470053837925,-0.8,-0.2));
#15211=CARTESIAN_POINT('',(-0.115470053837925,-0.5,-0.2));
#15212=CARTESIAN_POINT('',(0.115470053837925,-0.8,-0.2));
#15213=CARTESIAN_POINT('Origin',(-0.23094010767585,-0.5,-2.77555756156289E-17));
#15214=CARTESIAN_POINT('',(-0.23094010767585,-0.5,-2.82820063659975E-17));
#15215=CARTESIAN_POINT('',(-0.115470053837925,-0.5,-0.2));
#15216=CARTESIAN_POINT('',(-0.23094010767585,-0.8,-2.77555756156289E-17));
#15217=CARTESIAN_POINT('',(-0.23094010767585,-0.5,-2.82820063659975E-17));
#15218=CARTESIAN_POINT('',(-0.115470053837925,-0.8,-0.2));
#15219=CARTESIAN_POINT('Origin',(-0.115470053837925,-0.5,0.2));
#15220=CARTESIAN_POINT('',(-0.115470053837925,-0.5,0.2));
#15221=CARTESIAN_POINT('',(-0.23094010767585,-0.5,-2.82820063659975E-17));
#15222=CARTESIAN_POINT('',(-0.115470053837925,-0.8,0.2));
#15223=CARTESIAN_POINT('',(-0.115470053837925,-0.5,0.2));
#15224=CARTESIAN_POINT('',(-0.23094010767585,-0.8,-2.82820063659975E-17));
#15225=CARTESIAN_POINT('Origin',(0.115470053837925,-0.5,0.2));
#15226=CARTESIAN_POINT('',(0.115470053837925,-0.5,0.2));
#15227=CARTESIAN_POINT('',(-0.115470053837925,-0.5,0.2));
#15228=CARTESIAN_POINT('',(0.115470053837925,-0.8,0.2));
#15229=CARTESIAN_POINT('',(0.115470053837925,-0.5,0.2));
#15230=CARTESIAN_POINT('',(-0.115470053837925,-0.8,0.2));
#15231=CARTESIAN_POINT('Origin',(0.23094010767585,-0.5,0.));
#15232=CARTESIAN_POINT('',(0.115470053837925,-0.5,0.2));
#15233=CARTESIAN_POINT('',(0.115470053837925,-0.8,0.2));
#15234=CARTESIAN_POINT('Origin',(0.,-0.5,0.));
#15235=CARTESIAN_POINT('Origin',(0.,-0.8,0.));
#18917=UNCERTAINTY_MEASURE_WITH_UNIT(LENGTH_MEASURE(0.001),#19044,
'DISTANCE_ACCURACY_VALUE',
'Maximum model space distance between geometric entities at asserted c
onnectivities');
#18972=UNCERTAINTY_MEASURE_WITH_UNIT(LENGTH_MEASURE(0.001),#19044,
'DISTANCE_ACCURACY_VALUE',
'Maximum model space distance between geometric entities at asserted c
onnectivities');
#18988=(
GEOMETRIC_REPRESENTATION_CONTEXT(3)
GLOBAL_UNCERTAINTY_ASSIGNED_CONTEXT((#18917))
GLOBAL_UNIT_ASSIGNED_CONTEXT((#19044,#19046,#19047))
REPRESENTATION_CONTEXT('','3D')
);
#19043=(
GEOMETRIC_REPRESENTATION_CONTEXT(3)
GLOBAL_UNCERTAINTY_ASSIGNED_CONTEXT((#18972))
GLOBAL_UNIT_ASSIGNED_CONTEXT((#19044,#19046,#19047))
REPRESENTATION_CONTEXT('','3D')
);
#19044=(
LENGTH_UNIT()
NAMED_UNIT(*)
SI_UNIT(.CENTI.,.METRE.)
);
#19046=(
NAMED_UNIT(*)
PLANE_ANGLE_UNIT()
SI_UNIT($,.RADIAN.)
);
#19047=(
NAMED_UNIT(*)
SI_UNIT($,.STERADIAN.)
SOLID_ANGLE_UNIT()
);
#19063=SHAPE_DEFINITION_REPRESENTATION(#19133,#19321);
#19133=PRODUCT_DEFINITION_SHAPE('',$,#19392);
#19321=SHAPE_REPRESENTATION('',(#10477),#18988);
#19376=PRODUCT_DEFINITION_CONTEXT('part definition',#19588,'design');
#19392=PRODUCT_DEFINITION('2026-11-03-00-38-46-454','Cap Screw - M5x20',
#19462,#19376);
#19462=PRODUCT_DEFINITION_FORMATION('',$,#19605);
#19588=APPLICATION_CONTEXT(
'Core Data for Automotive Mechanical Design Process');
#19589=PRODUCT_CONTEXT('part definition',#19588,'mechanical');
#19605=PRODUCT('2026-11-03-00-38-46-454','Cap Screw - M5x20',
'Cap Screw - M5x20',(#19589));
#19663=PRESENTATION_STYLE_ASSIGNMENT((#19669));
#19669=SURFACE_STYLE_USAGE(.BOTH.,#19675);
#19675=SURFACE_SIDE_STYLE('',(#19681));
#19681=SURFACE_STYLE_FILL_AREA(#19687);
#19687=FILL_AREA_STYLE('CAD Library Painted - Graphite',(#19693));
#19693=FILL_AREA_STYLE_COLOUR('CAD Library Painted - Graphite',#19699);
#19699=COLOUR_RGB('CAD Library Painted - Graphite',0.168627450980392,0.192156862745098,
0.231372549019608);
ENDSEC;
END-ISO-10303-21;
